ISO-10303-21;
HEADER;
/* Generated by software containing ST-Developer
 * from STEP Tools, Inc. (www.steptools.com) 
 */

FILE_DESCRIPTION(
/* description */ ('Bin tilter linkage'),
/* implementation_level */ '2;1');

FILE_NAME(
/* name */ 'Foot (1).step',
/* time_stamp */ '2026-10-28T03:26:24-07:00',
/* author */ (''),
/* organization */ (''),
/* preprocessor_version */ 'ST-DEVELOPER v20.2',
/* originating_system */ 'Autodesk Translation Framework v15.17.0.0',
/* authorisation */ '');

FILE_SCHEMA (('AUTOMOTIVE_DESIGN { 1 0 10303 214 3 1 1 }'));
ENDSEC;

DATA;
#10=MECHANICAL_DESIGN_GEOMETRIC_PRESENTATION_REPRESENTATION('',(#864),#23728);
#652=SHAPE_REPRESENTATION_RELATIONSHIP('SRR','None',#24116,#758);
#758=ADVANCED_BREP_SHAPE_REPRESENTATION('',(#978),#23616);
#864=STYLED_ITEM('',(#24779),#978);
#978=MANIFOLD_SOLID_BREP('Body1',#12394);
#1504=PLANE('',#13729);
#1505=PLANE('',#13730);
#1506=PLANE('',#13731);
#1507=PLANE('',#13732);
#1508=PLANE('',#13733);
#1509=PLANE('',#13734);
#1914=FACE_OUTER_BOUND('',#2715,.T.);
#1915=FACE_OUTER_BOUND('',#2716,.T.);
#1916=FACE_OUTER_BOUND('',#2717,.T.);
#1917=FACE_OUTER_BOUND('',#2718,.T.);
#1918=FACE_OUTER_BOUND('',#2719,.T.);
#1919=FACE_OUTER_BOUND('',#2720,.T.);
#2715=EDGE_LOOP('',(#8493,#8494,#8495,#8496));
#2716=EDGE_LOOP('',(#8497,#8498,#8499,#8500));
#2717=EDGE_LOOP('',(#8501,#8502,#8503,#8504));
#2718=EDGE_LOOP('',(#8505,#8506,#8507,#8508));
#2719=EDGE_LOOP('',(#8509,#8510,#8511,#8512));
#2720=EDGE_LOOP('',(#8513,#8514,#8515,#8516));
#3885=LINE('',#19877,#4560);
#3886=LINE('',#19879,#4561);
#3887=LINE('',#19881,#4562);
#3888=LINE('',#19882,#4563);
#3889=LINE('',#19885,#4564);
#3890=LINE('',#19887,#4565);
#3891=LINE('',#19888,#4566);
#3892=LINE('',#19891,#4567);
#3893=LINE('',#19893,#4568);
#3894=LINE('',#19894,#4569);
#3895=LINE('',#19896,#4570);
#3896=LINE('',#19897,#4571);
#4560=VECTOR('',#15618,1.);
#4561=VECTOR('',#15619,1.);
#4562=VECTOR('',#15620,1.);
#4563=VECTOR('',#15621,1.);
#4564=VECTOR('',#15624,1.);
#4565=VECTOR('',#15625,1.);
#4566=VECTOR('',#15626,1.);
#4567=VECTOR('',#15629,1.);
#4568=VECTOR('',#15630,1.);
#4569=VECTOR('',#15631,1.);
#4570=VECTOR('',#15634,1.);
#4571=VECTOR('',#15635,1.);
#5997=VERTEX_POINT('',#19875);
#5998=VERTEX_POINT('',#19876);
#5999=VERTEX_POINT('',#19878);
#6000=VERTEX_POINT('',#19880);
#6001=VERTEX_POINT('',#19884);
#6002=VERTEX_POINT('',#19886);
#6003=VERTEX_POINT('',#19890);
#6004=VERTEX_POINT('',#19892);
#6986=EDGE_CURVE('',#5997,#5998,#3885,.T.);
#6987=EDGE_CURVE('',#5998,#5999,#3886,.T.);
#6988=EDGE_CURVE('',#6000,#5999,#3887,.T.);
#6989=EDGE_CURVE('',#5997,#6000,#3888,.T.);
#6990=EDGE_CURVE('',#6001,#5997,#3889,.T.);
#6991=EDGE_CURVE('',#6002,#6000,#3890,.T.);
#6992=EDGE_CURVE('',#6001,#6002,#3891,.T.);
#6993=EDGE_CURVE('',#6003,#6001,#3892,.T.);
#6994=EDGE_CURVE('',#6004,#6002,#3893,.T.);
#6995=EDGE_CURVE('',#6003,#6004,#3894,.T.);
#6996=EDGE_CURVE('',#5998,#6003,#3895,.T.);
#6997=EDGE_CURVE('',#5999,#6004,#3896,.T.);
#8493=ORIENTED_EDGE('',*,*,#6986,.T.);
#8494=ORIENTED_EDGE('',*,*,#6987,.T.);
#8495=ORIENTED_EDGE('',*,*,#6988,.F.);
#8496=ORIENTED_EDGE('',*,*,#6989,.F.);
#8497=ORIENTED_EDGE('',*,*,#6990,.T.);
#8498=ORIENTED_EDGE('',*,*,#6989,.T.);
#8499=ORIENTED_EDGE('',*,*,#6991,.F.);
#8500=ORIENTED_EDGE('',*,*,#6992,.F.);
#8501=ORIENTED_EDGE('',*,*,#6993,.T.);
#8502=ORIENTED_EDGE('',*,*,#6992,.T.);
#8503=ORIENTED_EDGE('',*,*,#6994,.F.);
#8504=ORIENTED_EDGE('',*,*,#6995,.F.);
#8505=ORIENTED_EDGE('',*,*,#6996,.T.);
#8506=ORIENTED_EDGE('',*,*,#6995,.T.);
#8507=ORIENTED_EDGE('',*,*,#6997,.F.);
#8508=ORIENTED_EDGE('',*,*,#6987,.F.);
#8509=ORIENTED_EDGE('',*,*,#6997,.T.);
#8510=ORIENTED_EDGE('',*,*,#6994,.T.);
#8511=ORIENTED_EDGE('',*,*,#6991,.T.);
#8512=ORIENTED_EDGE('',*,*,#6988,.T.);
#8513=ORIENTED_EDGE('',*,*,#6996,.F.);
#8514=ORIENTED_EDGE('',*,*,#6986,.F.);
#8515=ORIENTED_EDGE('',*,*,#6990,.F.);
#8516=ORIENTED_EDGE('',*,*,#6993,.F.);
#11639=ADVANCED_FACE('',(#1914),#1504,.T.);
#11640=ADVANCED_FACE('',(#1915),#1505,.T.);
#11641=ADVANCED_FACE('',(#1916),#1506,.T.);
#11642=ADVANCED_FACE('',(#1917),#1507,.T.);
#11643=ADVANCED_FACE('',(#1918),#1508,.T.);
#11644=ADVANCED_FACE('',(#1919),#1509,.F.);
#12394=CLOSED_SHELL('',(#11639,#11640,#11641,#11642,#11643,#11644));
#13728=AXIS2_PLACEMENT_3D('',#19873,#15614,#15615);
#13729=AXIS2_PLACEMENT_3D('',#19874,#15616,#15617);
#13730=AXIS2_PLACEMENT_3D('',#19883,#15622,#15623);
#13731=AXIS2_PLACEMENT_3D('',#19889,#15627,#15628);
#13732=AXIS2_PLACEMENT_3D('',#19895,#15632,#15633);
#13733=AXIS2_PLACEMENT_3D('',#19898,#15636,#15637);
#13734=AXIS2_PLACEMENT_3D('',#19899,#15638,#15639);
#15614=DIRECTION('axis',(0.,0.,1.));
#15615=DIRECTION('refdir',(1.,0.,0.));
#15616=DIRECTION('center_axis',(0.,1.,0.));
#15617=DIRECTION('ref_axis',(-1.,0.,0.));
#15618=DIRECTION('',(-1.,0.,0.));
#15619=DIRECTION('',(0.,0.,1.));
#15620=DIRECTION('',(-1.,0.,0.));
#15621=DIRECTION('',(0.,0.,1.));
#15622=DIRECTION('center_axis',(1.,0.,0.));
#15623=DIRECTION('ref_axis',(0.,1.,0.));
#15624=DIRECTION('',(0.,1.,0.));
#15625=DIRECTION('',(0.,1.,0.));
#15626=DIRECTION('',(0.,0.,1.));
#15627=DIRECTION('center_axis',(0.,-1.,0.));
#15628=DIRECTION('ref_axis',(1.,0.,0.));
#15629=DIRECTION('',(1.,0.,0.));
#15630=DIRECTION('',(1.,0.,0.));
#15631=DIRECTION('',(0.,0.,1.));
#15632=DIRECTION('center_axis',(-1.,0.,0.));
#15633=DIRECTION('ref_axis',(0.,-1.,0.));
#15634=DIRECTION('',(0.,-1.,0.));
#15635=DIRECTION('',(0.,-1.,0.));
#15636=DIRECTION('center_axis',(0.,0.,1.));
#15637=DIRECTION('ref_axis',(1.,0.,0.));
#15638=DIRECTION('center_axis',(0.,0.,1.));
#15639=DIRECTION('ref_axis',(1.,0.,0.));
#19873=CARTESIAN_POINT('',(0.,0.,0.));
#19874=CARTESIAN_POINT('Origin',(31.,10.,-0.8));
#19875=CARTESIAN_POINT('',(31.,10.,-0.8));
#19876=CARTESIAN_POINT('',(30.,10.,-0.8));
#19877=CARTESIAN_POINT('',(31.,10.,-0.8));
#19878=CARTESIAN_POINT('',(30.,10.,0.));
#19879=CARTESIAN_POINT('',(30.,10.,-0.8));
#19880=CARTESIAN_POINT('',(31.,10.,0.));
#19881=CARTESIAN_POINT('',(31.,10.,0.));
#19882=CARTESIAN_POINT('',(31.,10.,-0.8));
#19883=CARTESIAN_POINT('Origin',(31.,-10.,-0.8));
#19884=CARTESIAN_POINT('',(31.,-10.,-0.8));
#19885=CARTESIAN_POINT('',(31.,-10.,-0.8));
#19886=CARTESIAN_POINT('',(31.,-10.,0.));
#19887=CARTESIAN_POINT('',(31.,-10.,0.));
#19888=CARTESIAN_POINT('',(31.,-10.,-0.8));
#19889=CARTESIAN_POINT('Origin',(30.,-10.,-0.8));
#19890=CARTESIAN_POINT('',(30.,-10.,-0.8));
#19891=CARTESIAN_POINT('',(30.,-10.,-0.8));
#19892=CARTESIAN_POINT('',(30.,-10.,0.));
#19893=CARTESIAN_POINT('',(30.,-10.,0.));
#19894=CARTESIAN_POINT('',(30.,-10.,-0.8));
#19895=CARTESIAN_POINT('Origin',(30.,10.,-0.8));
#19896=CARTESIAN_POINT('',(30.,10.,-0.8));
#19897=CARTESIAN_POINT('',(30.,10.,0.));
#19898=CARTESIAN_POINT('Origin',(30.5,0.,0.));
#19899=CARTESIAN_POINT('Origin',(30.5,0.,-0.8));
#23499=UNCERTAINTY_MEASURE_WITH_UNIT(LENGTH_MEASURE(0.001),#23729,
'DISTANCE_ACCURACY_VALUE',
'Maximum model space distance between geometric entities at asserted c
onnectivities');
#23611=UNCERTAINTY_MEASURE_WITH_UNIT(LENGTH_MEASURE(0.001),#23729,
'DISTANCE_ACCURACY_VALUE',
'Maximum model space distance between geometric entities at asserted c
onnectivities');
#23616=(
GEOMETRIC_REPRESENTATION_CONTEXT(3)
GLOBAL_UNCERTAINTY_ASSIGNED_CONTEXT((#23499))
GLOBAL_UNIT_ASSIGNED_CONTEXT((#23729,#23731,#23732))
REPRESENTATION_CONTEXT('','3D')
);
#23728=(
GEOMETRIC_REPRESENTATION_CONTEXT(3)
GLOBAL_UNCERTAINTY_ASSIGNED_CONTEXT((#23611))
GLOBAL_UNIT_ASSIGNED_CONTEXT((#23729,#23731,#23732))
REPRESENTATION_CONTEXT('','3D')
);
#23729=(
LENGTH_UNIT()
NAMED_UNIT(*)
SI_UNIT(.CENTI.,.METRE.)
);
#23731=(
NAMED_UNIT(*)
PLANE_ANGLE_UNIT()
SI_UNIT($,.RADIAN.)
);
#23732=(
NAMED_UNIT(*)
SI_UNIT($,.STERADIAN.)
SOLID_ANGLE_UNIT()
);
#23737=SHAPE_DEFINITION_REPRESENTATION(#23853,#24116);
#23853=PRODUCT_DEFINITION_SHAPE('',$,#24233);
#24116=SHAPE_REPRESENTATION('',(#13728),#23616);
#24228=PRODUCT_DEFINITION_CONTEXT('part definition',#24578,'design');
#24233=PRODUCT_DEFINITION('Foot (1)','Foot (1)',#24349,#24228);
#24349=PRODUCT_DEFINITION_FORMATION('',$,#24584);
#24578=APPLICATION_CONTEXT(
'Core Data for Automotive Mechanical Design Process');
#24579=PRODUCT_CONTEXT('part definition',#24578,'mechanical');
#24584=PRODUCT('Foot (1)','Foot (1)','Foot (1)',(#24579));
#24773=COLOUR_RGB('Off White',0.89,0.88,0.83);
#24774=FILL_AREA_STYLE_COLOUR('',#24773);
#24775=FILL_AREA_STYLE('',(#24774));
#24776=SURFACE_STYLE_FILL_AREA(#24775);
#24777=SURFACE_SIDE_STYLE('',(#24776));
#24778=SURFACE_STYLE_USAGE(.BOTH.,#24777);
#24779=PRESENTATION_STYLE_ASSIGNMENT((#24778));
ENDSEC;
END-ISO-10303-21;
